ISO-10303-21;
HEADER;
/* Generated by software containing ST-Developer
 * from STEP Tools, Inc. (www.steptools.com) 
 */

FILE_DESCRIPTION(
/* description */ ('Crank-driven oscillating fan base (mechanism only)'),

/* implementation_level */ '2;1');

FILE_NAME(
/* name */ 'Shaft collar (1).step',
/* time_stamp */ '2026-10-28T03:25:00-07:00',
/* author */ (''),
/* organization */ (''),
/* preprocessor_version */ 'ST-DEVELOPER v20.2',
/* originating_system */ 'Autodesk Translation Framework v15.17.0.0',
/* authorisation */ '');

FILE_SCHEMA (('AUTOMOTIVE_DESIGN { 1 0 10303 214 3 1 1 }'));
ENDSEC;

DATA;
#10=MECHANICAL_DESIGN_GEOMETRIC_PRESENTATION_REPRESENTATION('',(#473),#11916);
#352=B_SPLINE_CURVE_WITH_KNOTS('',3,(#11321,#11322,#11323,#11324,#11325,
#11326,#11327,#11328,#11329,#11330,#11331,#11332,#11333,#11334),
 .UNSPECIFIED.,.F.,.F.,(4,2,2,2,2,2,4),(0.618551524396289,0.626563103102765,
0.689203386094988,0.751843669087211,0.814483952079434,0.877124235071657,
0.885135813778134),.UNSPECIFIED.);
#353=B_SPLINE_CURVE_WITH_KNOTS('',3,(#11338,#11339,#11340,#11341,#11342,
#11343,#11344,#11345),.UNSPECIFIED.,.F.,.F.,(4,2,2,4),(0.250614556362404,
0.313254839354627,0.37589512234685,0.383906701053326),.UNSPECIFIED.);
#354=B_SPLINE_CURVE_WITH_KNOTS('',3,(#11349,#11350,#11351,#11352,#11353,
#11354,#11355,#11356,#11357,#11358,#11359,#11360,#11361,#11362,#11363,#11364,
#11365,#11366,#11367,#11368,#11369,#11370,#11371,#11372,#11373,#11374),
 .UNSPECIFIED.,.F.,.F.,(4,2,2,2,2,2,2,2,2,2,2,2,4),(0.,0.0623062782223143,
0.124612556444629,0.186916384615149,0.249220212785669,0.31152404095619,
0.37382786912671,0.436134147349024,0.498440425571339,0.560746703793653,
0.623052982015967,0.685356810186488,0.747660638357008),.UNSPECIFIED.);
#355=B_SPLINE_CURVE_WITH_KNOTS('',3,(#11375,#11376,#11377,#11378,#11379,
#11380,#11381,#11382,#11383,#11384),.UNSPECIFIED.,.F.,.F.,(4,2,2,2,4),(0.747660638357008,
0.809964466527529,0.872268294698049,0.934574572920363,0.996880851142677),
 .UNSPECIFIED.);
#356=B_SPLINE_CURVE_WITH_KNOTS('',3,(#11385,#11386,#11387,#11388,#11389,
#11390,#11391,#11392),.UNSPECIFIED.,.F.,.F.,(4,2,2,4),(0.117322411671481,
0.125333990377958,0.187974273370181,0.250614556362404),.UNSPECIFIED.);
#385=SHAPE_REPRESENTATION_RELATIONSHIP('SRR','None',#12112,#425);
#425=ADVANCED_BREP_SHAPE_REPRESENTATION('',(#520),#11903);
#473=STYLED_ITEM('',(#12375),#520);
#520=MANIFOLD_SOLID_BREP('Body1',#6104);
#665=FACE_BOUND('',#1681,.T.);
#666=FACE_BOUND('',#1683,.T.);
#667=FACE_BOUND('',#1685,.T.);
#668=FACE_BOUND('',#1687,.T.);
#829=PLANE('',#7178);
#830=PLANE('',#7182);
#831=PLANE('',#7189);
#832=PLANE('',#7190);
#1167=FACE_OUTER_BOUND('',#1677,.T.);
#1168=FACE_OUTER_BOUND('',#1678,.T.);
#1169=FACE_OUTER_BOUND('',#1679,.T.);
#1170=FACE_OUTER_BOUND('',#1680,.T.);
#1171=FACE_OUTER_BOUND('',#1682,.T.);
#1172=FACE_OUTER_BOUND('',#1684,.T.);
#1173=FACE_OUTER_BOUND('',#1686,.T.);
#1677=EDGE_LOOP('',(#5206,#5207));
#1678=EDGE_LOOP('',(#5208,#5209,#5210,#5211,#5212,#5213,#5214,#5215,#5216));
#1679=EDGE_LOOP('',(#5217,#5218));
#1680=EDGE_LOOP('',(#5219,#5220,#5221,#5222));
#1681=EDGE_LOOP('',(#5223,#5224,#5225,#5226,#5227));
#1682=EDGE_LOOP('',(#5228,#5229,#5230,#5231));
#1683=EDGE_LOOP('',(#5232,#5233));
#1684=EDGE_LOOP('',(#5234));
#1685=EDGE_LOOP('',(#5235));
#1686=EDGE_LOOP('',(#5236));
#1687=EDGE_LOOP('',(#5237));
#2032=LINE('',#11317,#2365);
#2033=LINE('',#11347,#2366);
#2034=LINE('',#11394,#2367);
#2035=LINE('',#11399,#2368);
#2036=LINE('',#11405,#2369);
#2365=VECTOR('',#8885,1.);
#2366=VECTOR('',#8892,0.165);
#2367=VECTOR('',#8895,1.);
#2368=VECTOR('',#8900,0.505000000000001);
#2369=VECTOR('',#8907,0.9);
#2763=CIRCLE('',#7179,0.165);
#2764=CIRCLE('',#7181,0.165);
#2765=CIRCLE('',#7184,0.505000000000001);
#2766=CIRCLE('',#7185,0.505000000000001);
#2767=CIRCLE('',#7187,0.9);
#2768=CIRCLE('',#7188,0.9);
#3218=VERTEX_POINT('',#11315);
#3219=VERTEX_POINT('',#11316);
#3220=VERTEX_POINT('',#11320);
#3221=VERTEX_POINT('',#11335);
#3222=VERTEX_POINT('',#11337);
#3223=VERTEX_POINT('',#11346);
#3224=VERTEX_POINT('',#11348);
#3225=VERTEX_POINT('',#11396);
#3226=VERTEX_POINT('',#11398);
#3227=VERTEX_POINT('',#11402);
#3228=VERTEX_POINT('',#11404);
#3898=EDGE_CURVE('',#3218,#3219,#2032,.T.);
#3899=EDGE_CURVE('',#3218,#3219,#2763,.T.);
#3900=EDGE_CURVE('',#3220,#3218,#352,.T.);
#3901=EDGE_CURVE('',#3221,#3220,#2764,.T.);
#3902=EDGE_CURVE('',#3222,#3221,#353,.T.);
#3903=EDGE_CURVE('',#3222,#3223,#2033,.T.);
#3904=EDGE_CURVE('',#3224,#3223,#354,.T.);
#3905=EDGE_CURVE('',#3223,#3224,#355,.T.);
#3906=EDGE_CURVE('',#3219,#3222,#356,.T.);
#3907=EDGE_CURVE('',#3221,#3220,#2034,.T.);
#3908=EDGE_CURVE('',#3225,#3225,#2765,.T.);
#3909=EDGE_CURVE('',#3225,#3226,#2035,.T.);
#3910=EDGE_CURVE('',#3226,#3226,#2766,.T.);
#3911=EDGE_CURVE('',#3227,#3227,#2767,.T.);
#3912=EDGE_CURVE('',#3227,#3228,#2036,.T.);
#3913=EDGE_CURVE('',#3228,#3228,#2768,.T.);
#5206=ORIENTED_EDGE('',*,*,#3898,.F.);
#5207=ORIENTED_EDGE('',*,*,#3899,.T.);
#5208=ORIENTED_EDGE('',*,*,#3900,.F.);
#5209=ORIENTED_EDGE('',*,*,#3901,.F.);
#5210=ORIENTED_EDGE('',*,*,#3902,.F.);
#5211=ORIENTED_EDGE('',*,*,#3903,.T.);
#5212=ORIENTED_EDGE('',*,*,#3904,.F.);
#5213=ORIENTED_EDGE('',*,*,#3905,.F.);
#5214=ORIENTED_EDGE('',*,*,#3903,.F.);
#5215=ORIENTED_EDGE('',*,*,#3906,.F.);
#5216=ORIENTED_EDGE('',*,*,#3899,.F.);
#5217=ORIENTED_EDGE('',*,*,#3907,.F.);
#5218=ORIENTED_EDGE('',*,*,#3901,.T.);
#5219=ORIENTED_EDGE('',*,*,#3908,.F.);
#5220=ORIENTED_EDGE('',*,*,#3909,.T.);
#5221=ORIENTED_EDGE('',*,*,#3910,.T.);
#5222=ORIENTED_EDGE('',*,*,#3909,.F.);
#5223=ORIENTED_EDGE('',*,*,#3906,.T.);
#5224=ORIENTED_EDGE('',*,*,#3902,.T.);
#5225=ORIENTED_EDGE('',*,*,#3907,.T.);
#5226=ORIENTED_EDGE('',*,*,#3900,.T.);
#5227=ORIENTED_EDGE('',*,*,#3898,.T.);
#5228=ORIENTED_EDGE('',*,*,#3911,.F.);
#5229=ORIENTED_EDGE('',*,*,#3912,.T.);
#5230=ORIENTED_EDGE('',*,*,#3913,.T.);
#5231=ORIENTED_EDGE('',*,*,#3912,.F.);
#5232=ORIENTED_EDGE('',*,*,#3904,.T.);
#5233=ORIENTED_EDGE('',*,*,#3905,.T.);
#5234=ORIENTED_EDGE('',*,*,#3911,.T.);
#5235=ORIENTED_EDGE('',*,*,#3908,.T.);
#5236=ORIENTED_EDGE('',*,*,#3913,.F.);
#5237=ORIENTED_EDGE('',*,*,#3910,.F.);
#5663=CYLINDRICAL_SURFACE('',#7180,0.165);
#5664=CYLINDRICAL_SURFACE('',#7183,0.505000000000001);
#5665=CYLINDRICAL_SURFACE('',#7186,0.9);
#5973=ADVANCED_FACE('',(#1167),#829,.T.);
#5974=ADVANCED_FACE('',(#1168),#5663,.F.);
#5975=ADVANCED_FACE('',(#1169),#830,.T.);
#5976=ADVANCED_FACE('',(#1170,#665),#5664,.F.);
#5977=ADVANCED_FACE('',(#1171,#666),#5665,.T.);
#5978=ADVANCED_FACE('',(#1172,#667),#831,.T.);
#5979=ADVANCED_FACE('',(#1173,#668),#832,.F.);
#6104=CLOSED_SHELL('',(#5973,#5974,#5975,#5976,#5977,#5978,#5979));
#7177=AXIS2_PLACEMENT_3D('',#11313,#8881,#8882);
#7178=AXIS2_PLACEMENT_3D('',#11314,#8883,#8884);
#7179=AXIS2_PLACEMENT_3D('',#11318,#8886,#8887);
#7180=AXIS2_PLACEMENT_3D('',#11319,#8888,#8889);
#7181=AXIS2_PLACEMENT_3D('',#11336,#8890,#8891);
#7182=AXIS2_PLACEMENT_3D('',#11393,#8893,#8894);
#7183=AXIS2_PLACEMENT_3D('',#11395,#8896,#8897);
#7184=AXIS2_PLACEMENT_3D('',#11397,#8898,#8899);
#7185=AXIS2_PLACEMENT_3D('',#11400,#8901,#8902);
#7186=AXIS2_PLACEMENT_3D('',#11401,#8903,#8904);
#7187=AXIS2_PLACEMENT_3D('',#11403,#8905,#8906);
#7188=AXIS2_PLACEMENT_3D('',#11406,#8908,#8909);
#7189=AXIS2_PLACEMENT_3D('',#11407,#8910,#8911);
#7190=AXIS2_PLACEMENT_3D('',#11408,#8912,#8913);
#8881=DIRECTION('axis',(0.,0.,1.));
#8882=DIRECTION('refdir',(1.,0.,0.));
#8883=DIRECTION('center_axis',(1.,0.,0.));
#8884=DIRECTION('ref_axis',(0.,0.,-1.));
#8885=DIRECTION('',(0.,0.,1.));
#8886=DIRECTION('center_axis',(1.,0.,0.));
#8887=DIRECTION('ref_axis',(0.,0.,-1.));
#8888=DIRECTION('center_axis',(1.,0.,0.));
#8889=DIRECTION('ref_axis',(0.,0.,-1.));
#8890=DIRECTION('center_axis',(1.,0.,0.));
#8891=DIRECTION('ref_axis',(0.,0.,-1.));
#8892=DIRECTION('',(1.,0.,0.));
#8893=DIRECTION('center_axis',(1.,0.,0.));
#8894=DIRECTION('ref_axis',(0.,0.,-1.));
#8895=DIRECTION('',(0.,0.,-1.));
#8896=DIRECTION('center_axis',(0.,0.,1.));
#8897=DIRECTION('ref_axis',(1.,0.,0.));
#8898=DIRECTION('center_axis',(0.,0.,-1.));
#8899=DIRECTION('ref_axis',(1.,0.,0.));
#8900=DIRECTION('',(0.,0.,-1.));
#8901=DIRECTION('center_axis',(0.,0.,-1.));
#8902=DIRECTION('ref_axis',(1.,0.,0.));
#8903=DIRECTION('center_axis',(0.,0.,1.));
#8904=DIRECTION('ref_axis',(1.,0.,0.));
#8905=DIRECTION('center_axis',(0.,0.,1.));
#8906=DIRECTION('ref_axis',(1.,0.,0.));
#8907=DIRECTION('',(0.,0.,-1.));
#8908=DIRECTION('center_axis',(0.,0.,1.));
#8909=DIRECTION('ref_axis',(1.,0.,0.));
#8910=DIRECTION('center_axis',(0.,0.,1.));
#8911=DIRECTION('ref_axis',(1.,0.,0.));
#8912=DIRECTION('center_axis',(0.,0.,1.));
#8913=DIRECTION('ref_axis',(1.,0.,0.));
#11313=CARTESIAN_POINT('',(0.,0.,0.));
#11314=CARTESIAN_POINT('Origin',(8.49,0.,1.4));
#11315=CARTESIAN_POINT('',(8.49,0.122167917228709,1.28909463493591));
#11316=CARTESIAN_POINT('',(8.49,0.122167917228709,1.51090536506409));
#11317=CARTESIAN_POINT('',(8.49,0.122167917228709,1.));
#11318=CARTESIAN_POINT('Origin',(8.49,0.,1.4));
#11319=CARTESIAN_POINT('Origin',(8.49,0.,1.4));
#11320=CARTESIAN_POINT('',(8.49,-0.122167917228709,1.28909463493591));
#11321=CARTESIAN_POINT('Ctrl Pts',(8.49,-0.122167917228708,1.28909463493591));
#11322=CARTESIAN_POINT('Ctrl Pts',(8.49044853167999,-0.120368913626297,
1.28711294069536));
#11323=CARTESIAN_POINT('Ctrl Pts',(8.49089524537169,-0.118534896565232,
1.28518965877367));
#11324=CARTESIAN_POINT('Ctrl Pts',(8.49479501553165,-0.102111993019358,
1.2687667552278));
#11325=CARTESIAN_POINT('Ctrl Pts',(8.49844251460759,-0.0836597150224316,
1.25609154388858));
#11326=CARTESIAN_POINT('Ctrl Pts',(8.50357781976106,-0.0430495960471594,
1.23920409039234));
#11327=CARTESIAN_POINT('Ctrl Pts',(8.505,-0.020880094330741,1.235));
#11328=CARTESIAN_POINT('Ctrl Pts',(8.505,0.020880094330741,1.235));
#11329=CARTESIAN_POINT('Ctrl Pts',(8.50357781976106,0.0430495960471594,
1.23920409039234));
#11330=CARTESIAN_POINT('Ctrl Pts',(8.49844251460759,0.0836597150224316,
1.25609154388858));
#11331=CARTESIAN_POINT('Ctrl Pts',(8.49479501553165,0.102111993019358,1.2687667552278));
#11332=CARTESIAN_POINT('Ctrl Pts',(8.49089524537169,0.118534896565232,1.28518965877367));
#11333=CARTESIAN_POINT('Ctrl Pts',(8.49044853167999,0.120368913626297,1.28711294069536));
#11334=CARTESIAN_POINT('Ctrl Pts',(8.49,0.122167917228708,1.28909463493591));
#11335=CARTESIAN_POINT('',(8.49,-0.122167917228709,1.51090536506409));
#11336=CARTESIAN_POINT('Origin',(8.49,0.,1.4));
#11337=CARTESIAN_POINT('',(8.505,-2.05116769488265E-17,1.565));
#11338=CARTESIAN_POINT('Ctrl Pts',(8.505,-2.08166817117217E-17,1.565));
#11339=CARTESIAN_POINT('Ctrl Pts',(8.505,-0.020880094330741,1.565));
#11340=CARTESIAN_POINT('Ctrl Pts',(8.50357781976106,-0.0430495960471594,
1.56079590960766));
#11341=CARTESIAN_POINT('Ctrl Pts',(8.49844251460759,-0.0836597150224316,
1.54390845611142));
#11342=CARTESIAN_POINT('Ctrl Pts',(8.49479501553165,-0.102111993019358,
1.5312332447722));
#11343=CARTESIAN_POINT('Ctrl Pts',(8.49089524537169,-0.118534896565232,
1.51481034122633));
#11344=CARTESIAN_POINT('Ctrl Pts',(8.49044853167999,-0.120368913626297,
1.51288705930464));
#11345=CARTESIAN_POINT('Ctrl Pts',(8.49,-0.122167917228708,1.51090536506409));
#11346=CARTESIAN_POINT('',(8.9,-2.02066721859313E-17,1.565));
#11347=CARTESIAN_POINT('',(8.49,-2.02066721859313E-17,1.565));
#11348=CARTESIAN_POINT('',(8.88474572618352,0.165,1.4));
#11349=CARTESIAN_POINT('Ctrl Pts',(8.88474572618352,0.165,1.4));
#11350=CARTESIAN_POINT('Ctrl Pts',(8.88474572618352,0.165,1.37923124059256));
#11351=CARTESIAN_POINT('Ctrl Pts',(8.88555275950526,0.160839719007584,1.35711110492666));
#11352=CARTESIAN_POINT('Ctrl Pts',(8.88844864815004,0.143986470216691,1.31647293736623));
#11353=CARTESIAN_POINT('Ctrl Pts',(8.89049360485164,0.131295993814186,1.29795075602263));
#11354=CARTESIAN_POINT('Ctrl Pts',(8.89431723432394,0.102049819008125,1.26870458121656));
#11355=CARTESIAN_POINT('Ctrl Pts',(8.89634708889954,0.0835273920906824,
1.25601365401642));
#11356=CARTESIAN_POINT('Ctrl Pts',(8.89920827186059,0.0428883760934127,
1.23916007816136));
#11357=CARTESIAN_POINT('Ctrl Pts',(8.9,0.0207679427235068,1.235));
#11358=CARTESIAN_POINT('Ctrl Pts',(8.9,-0.0207679427235068,1.235));
#11359=CARTESIAN_POINT('Ctrl Pts',(8.89920827186059,-0.0428883760934129,
1.23916007816136));
#11360=CARTESIAN_POINT('Ctrl Pts',(8.89634708889954,-0.0835273920906825,
1.25601365401642));
#11361=CARTESIAN_POINT('Ctrl Pts',(8.89431723432394,-0.102049819008125,
1.26870458121656));
#11362=CARTESIAN_POINT('Ctrl Pts',(8.89049360485164,-0.131295993814186,
1.29795075602263));
#11363=CARTESIAN_POINT('Ctrl Pts',(8.88844864815004,-0.143986470216691,
1.31647293736623));
#11364=CARTESIAN_POINT('Ctrl Pts',(8.88555275950526,-0.160839719007584,
1.35711110492666));
#11365=CARTESIAN_POINT('Ctrl Pts',(8.88474572618352,-0.165,1.37923124059256));
#11366=CARTESIAN_POINT('Ctrl Pts',(8.88474572618352,-0.165,1.42076875940744));
#11367=CARTESIAN_POINT('Ctrl Pts',(8.88555275950526,-0.160839719007584,
1.44288889507334));
#11368=CARTESIAN_POINT('Ctrl Pts',(8.88844864815004,-0.143986470216691,
1.48352706263377));
#11369=CARTESIAN_POINT('Ctrl Pts',(8.89049360485164,-0.131295993814186,
1.50204924397737));
#11370=CARTESIAN_POINT('Ctrl Pts',(8.89431723432394,-0.102049819008125,
1.53129541878344));
#11371=CARTESIAN_POINT('Ctrl Pts',(8.89634708889954,-0.0835273920906824,
1.54398634598358));
#11372=CARTESIAN_POINT('Ctrl Pts',(8.89920827186059,-0.0428883760934127,
1.56083992183864));
#11373=CARTESIAN_POINT('Ctrl Pts',(8.9,-0.0207679427235068,1.565));
#11374=CARTESIAN_POINT('Ctrl Pts',(8.9,-2.08166817117217E-17,1.565));
#11375=CARTESIAN_POINT('Ctrl Pts',(8.9,-2.77555756156289E-17,1.565));
#11376=CARTESIAN_POINT('Ctrl Pts',(8.9,0.0207679427235068,1.565));
#11377=CARTESIAN_POINT('Ctrl Pts',(8.89920827186059,0.0428883760934128,
1.56083992183864));
#11378=CARTESIAN_POINT('Ctrl Pts',(8.89634708889954,0.0835273920906824,
1.54398634598358));
#11379=CARTESIAN_POINT('Ctrl Pts',(8.89431723432394,0.102049819008125,1.53129541878344));
#11380=CARTESIAN_POINT('Ctrl Pts',(8.89049360485164,0.131295993814186,1.50204924397737));
#11381=CARTESIAN_POINT('Ctrl Pts',(8.88844864815004,0.143986470216691,1.48352706263377));
#11382=CARTESIAN_POINT('Ctrl Pts',(8.88555275950526,0.160839719007584,1.44288889507334));
#11383=CARTESIAN_POINT('Ctrl Pts',(8.88474572618352,0.165,1.42076875940744));
#11384=CARTESIAN_POINT('Ctrl Pts',(8.88474572618352,0.165,1.4));
#11385=CARTESIAN_POINT('Ctrl Pts',(8.49,0.122167917228708,1.51090536506409));
#11386=CARTESIAN_POINT('Ctrl Pts',(8.49044853167999,0.120368913626297,1.51288705930464));
#11387=CARTESIAN_POINT('Ctrl Pts',(8.49089524537169,0.118534896565232,1.51481034122633));
#11388=CARTESIAN_POINT('Ctrl Pts',(8.49479501553165,0.102111993019358,1.5312332447722));
#11389=CARTESIAN_POINT('Ctrl Pts',(8.49844251460759,0.0836597150224316,
1.54390845611142));
#11390=CARTESIAN_POINT('Ctrl Pts',(8.50357781976106,0.0430495960471594,
1.56079590960766));
#11391=CARTESIAN_POINT('Ctrl Pts',(8.505,0.0208800943307409,1.565));
#11392=CARTESIAN_POINT('Ctrl Pts',(8.505,-6.93889390390723E-17,1.565));
#11393=CARTESIAN_POINT('Origin',(8.49,0.,1.4));
#11394=CARTESIAN_POINT('',(8.49,-0.122167917228709,1.));
#11395=CARTESIAN_POINT('Origin',(8.,0.,1.));
#11396=CARTESIAN_POINT('',(7.495,-6.18446633569414E-17,1.8));
#11397=CARTESIAN_POINT('Origin',(8.,0.,1.8));
#11398=CARTESIAN_POINT('',(7.495,-6.18446633569414E-17,1.));
#11399=CARTESIAN_POINT('',(7.495,-6.18446633569414E-17,1.));
#11400=CARTESIAN_POINT('Origin',(8.,0.,1.));
#11401=CARTESIAN_POINT('Origin',(8.,0.,1.));
#11402=CARTESIAN_POINT('',(7.1,-1.10218211923262E-16,1.8));
#11403=CARTESIAN_POINT('Origin',(8.,0.,1.8));
#11404=CARTESIAN_POINT('',(7.1,-1.10218211923262E-16,1.));
#11405=CARTESIAN_POINT('',(7.1,-1.10218211923262E-16,1.));
#11406=CARTESIAN_POINT('Origin',(8.,0.,1.));
#11407=CARTESIAN_POINT('Origin',(8.,0.,1.8));
#11408=CARTESIAN_POINT('Origin',(8.,0.,1.));
#11856=UNCERTAINTY_MEASURE_WITH_UNIT(LENGTH_MEASURE(0.001),#11917,
'DISTANCE_ACCURACY_VALUE',
'Maximum model space distance between geometric entities at asserted c
onnectivities');
#11869=UNCERTAINTY_MEASURE_WITH_UNIT(LENGTH_MEASURE(0.001),#11917,
'DISTANCE_ACCURACY_VALUE',
'Maximum model space distance between geometric entities at asserted c
onnectivities');
#11903=(
GEOMETRIC_REPRESENTATION_CONTEXT(3)
GLOBAL_UNCERTAINTY_ASSIGNED_CONTEXT((#11856))
GLOBAL_UNIT_ASSIGNED_CONTEXT((#11917,#11919,#11920))
REPRESENTATION_CONTEXT('','3D')
);
#11916=(
GEOMETRIC_REPRESENTATION_CONTEXT(3)
GLOBAL_UNCERTAINTY_ASSIGNED_CONTEXT((#11869))
GLOBAL_UNIT_ASSIGNED_CONTEXT((#11917,#11919,#11920))
REPRESENTATION_CONTEXT('','3D')
);
#11917=(
LENGTH_UNIT()
NAMED_UNIT(*)
SI_UNIT(.CENTI.,.METRE.)
);
#11919=(
NAMED_UNIT(*)
PLANE_ANGLE_UNIT()
SI_UNIT($,.RADIAN.)
);
#11920=(
NAMED_UNIT(*)
SI_UNIT($,.STERADIAN.)
SOLID_ANGLE_UNIT()
);
#11954=SHAPE_DEFINITION_REPRESENTATION(#12005,#12112);
#12005=PRODUCT_DEFINITION_SHAPE('',$,#12159);
#12112=SHAPE_REPRESENTATION('',(#7177),#11903);
#12125=PRODUCT_DEFINITION_CONTEXT('part definition',#12265,'design');
#12159=PRODUCT_DEFINITION('Shaft collar (1)','Shaft collar (1)',#12205,#12125);
#12205=PRODUCT_DEFINITION_FORMATION('',$,#12300);
#12265=APPLICATION_CONTEXT(
'Core Data for Automotive Mechanical Design Process');
#12266=PRODUCT_CONTEXT('part definition',#12265,'mechanical');
#12300=PRODUCT('Shaft collar (1)','Shaft collar (1)','Shaft collar (1)',(#12266));
#12369=COLOUR_RGB('Grey',0.48,0.52,0.57);
#12370=FILL_AREA_STYLE_COLOUR('',#12369);
#12371=FILL_AREA_STYLE('',(#12370));
#12372=SURFACE_STYLE_FILL_AREA(#12371);
#12373=SURFACE_SIDE_STYLE('',(#12372));
#12374=SURFACE_STYLE_USAGE(.BOTH.,#12373);
#12375=PRESENTATION_STYLE_ASSIGNMENT((#12374));
ENDSEC;
END-ISO-10303-21;
